ISO-10303-21;
HEADER;
/* Generated by software containing ST-Developer
 * from STEP Tools, Inc. (www.steptools.com) 
 */

FILE_DESCRIPTION(
/* description */ ('STEP AP214'),
/* implementation_level */ '2;1');

FILE_NAME(
/* name */ 'Socket Head Cap Screw M6x25.step',
/* time_stamp */ '2026-11-15T14:49:54-08:00',
/* author */ (''),
/* organization */ (''),
/* preprocessor_version */ 'ST-DEVELOPER v20.2',
/* originating_system */ 'Autodesk Translation Framework v15.17.0.0',
/* authorisation */ '');

FILE_SCHEMA (('AUTOMOTIVE_DESIGN { 1 0 10303 214 3 1 1 }'));
ENDSEC;

DATA;
#10=MECHANICAL_DESIGN_GEOMETRIC_PRESENTATION_REPRESENTATION('',(#1132),#66721);
#580=CONICAL_SURFACE('',#28684,5.,0.785398163397451);
#581=CONICAL_SURFACE('',#28686,2.4585,0.785398163397442);
#1066=SHAPE_REPRESENTATION_RELATIONSHIP('SRR','None',#66929,#1097);
#1097=ADVANCED_BREP_SHAPE_REPRESENTATION('',(#1167),#66720);
#1132=STYLED_ITEM('',(#67095),#1167);
#1167=MANIFOLD_SOLID_BREP('Body1',#25698);
#1496=FACE_BOUND('',#5473,.T.);
#1497=FACE_BOUND('',#5475,.T.);
#2259=PLANE('',#28692);
#2260=PLANE('',#28693);
#2261=PLANE('',#28694);
#2262=PLANE('',#28695);
#2263=PLANE('',#28696);
#2264=PLANE('',#28697);
#2265=PLANE('',#28698);
#2266=PLANE('',#28699);
#2267=PLANE('',#28700);
#2268=PLANE('',#28701);
#3697=FACE_OUTER_BOUND('',#5467,.T.);
#3698=FACE_OUTER_BOUND('',#5468,.T.);
#3699=FACE_OUTER_BOUND('',#5469,.T.);
#3700=FACE_OUTER_BOUND('',#5470,.T.);
#3701=FACE_OUTER_BOUND('',#5471,.T.);
#3702=FACE_OUTER_BOUND('',#5472,.T.);
#3703=FACE_OUTER_BOUND('',#5474,.T.);
#3704=FACE_OUTER_BOUND('',#5476,.T.);
#3705=FACE_OUTER_BOUND('',#5477,.T.);
#3706=FACE_OUTER_BOUND('',#5478,.T.);
#3707=FACE_OUTER_BOUND('',#5479,.T.);
#3708=FACE_OUTER_BOUND('',#5480,.T.);
#3709=FACE_OUTER_BOUND('',#5481,.T.);
#3710=FACE_OUTER_BOUND('',#5482,.T.);
#5467=EDGE_LOOP('',(#23744,#23745,#23746,#23747));
#5468=EDGE_LOOP('',(#23748,#23749,#23750,#23751));
#5469=EDGE_LOOP('',(#23752,#23753,#23754,#23755,#23756));
#5470=EDGE_LOOP('',(#23757,#23758,#23759,#23760,#23761));
#5471=EDGE_LOOP('',(#23762));
#5472=EDGE_LOOP('',(#23763));
#5473=EDGE_LOOP('',(#23764,#23765,#23766,#23767,#23768,#23769));
#5474=EDGE_LOOP('',(#23770));
#5475=EDGE_LOOP('',(#23771));
#5476=EDGE_LOOP('',(#23772,#23773,#23774,#23775));
#5477=EDGE_LOOP('',(#23776,#23777,#23778,#23779));
#5478=EDGE_LOOP('',(#23780,#23781,#23782,#23783));
#5479=EDGE_LOOP('',(#23784,#23785,#23786,#23787));
#5480=EDGE_LOOP('',(#23788,#23789,#23790,#23791));
#5481=EDGE_LOOP('',(#23792,#23793,#23794,#23795));
#5482=EDGE_LOOP('',(#23796,#23797,#23798,#23799,#23800,#23801));
#7450=LINE('',#66528,#9439);
#7451=LINE('',#66532,#9440);
#7452=LINE('',#66539,#9441);
#7453=LINE('',#66544,#9442);
#7454=LINE('',#66550,#9443);
#7455=LINE('',#66552,#9444);
#7456=LINE('',#66554,#9445);
#7457=LINE('',#66556,#9446);
#7458=LINE('',#66558,#9447);
#7459=LINE('',#66559,#9448);
#7460=LINE('',#66563,#9449);
#7461=LINE('',#66565,#9450);
#7462=LINE('',#66566,#9451);
#7463=LINE('',#66569,#9452);
#7464=LINE('',#66570,#9453);
#7465=LINE('',#66573,#9454);
#7466=LINE('',#66574,#9455);
#7467=LINE('',#66577,#9456);
#7468=LINE('',#66578,#9457);
#7469=LINE('',#66581,#9458);
#7470=LINE('',#66582,#9459);
#7471=LINE('',#66584,#9460);
#9439=VECTOR('',#36007,5.);
#9440=VECTOR('',#36012,5.);
#9441=VECTOR('',#36019,2.4585);
#9442=VECTOR('',#36026,3.);
#9443=VECTOR('',#36033,1000.);
#9444=VECTOR('',#36034,1000.);
#9445=VECTOR('',#36035,1000.);
#9446=VECTOR('',#36036,1000.);
#9447=VECTOR('',#36037,1000.);
#9448=VECTOR('',#36038,1000.);
#9449=VECTOR('',#36043,1000.);
#9450=VECTOR('',#36044,1000.);
#9451=VECTOR('',#36045,1000.);
#9452=VECTOR('',#36048,1000.);
#9453=VECTOR('',#36049,1000.);
#9454=VECTOR('',#36052,1000.);
#9455=VECTOR('',#36053,1000.);
#9456=VECTOR('',#36056,1000.);
#9457=VECTOR('',#36057,1000.);
#9458=VECTOR('',#36060,1000.);
#9459=VECTOR('',#36061,1000.);
#9460=VECTOR('',#36064,1000.);
#10631=CIRCLE('',#28682,5.);
#10632=CIRCLE('',#28683,5.);
#10633=CIRCLE('',#28685,4.4);
#10634=CIRCLE('',#28687,3.);
#10635=CIRCLE('',#28688,2.4585);
#10636=CIRCLE('',#28689,3.);
#10637=CIRCLE('',#28691,3.);
#12971=VERTEX_POINT('',#66525);
#12972=VERTEX_POINT('',#66527);
#12973=VERTEX_POINT('',#66531);
#12974=VERTEX_POINT('',#66535);
#12975=VERTEX_POINT('',#66536);
#12976=VERTEX_POINT('',#66538);
#12977=VERTEX_POINT('',#66543);
#12978=VERTEX_POINT('',#66548);
#12979=VERTEX_POINT('',#66549);
#12980=VERTEX_POINT('',#66551);
#12981=VERTEX_POINT('',#66553);
#12982=VERTEX_POINT('',#66555);
#12983=VERTEX_POINT('',#66557);
#12984=VERTEX_POINT('',#66562);
#12985=VERTEX_POINT('',#66564);
#12986=VERTEX_POINT('',#66568);
#12987=VERTEX_POINT('',#66572);
#12988=VERTEX_POINT('',#66576);
#12989=VERTEX_POINT('',#66580);
#16565=EDGE_CURVE('',#12971,#12971,#10631,.T.);
#16566=EDGE_CURVE('',#12971,#12972,#7450,.T.);
#16567=EDGE_CURVE('',#12972,#12972,#10632,.T.);
#16568=EDGE_CURVE('',#12972,#12973,#7451,.T.);
#16569=EDGE_CURVE('',#12973,#12973,#10633,.T.);
#16570=EDGE_CURVE('',#12974,#12975,#10634,.T.);
#16571=EDGE_CURVE('',#12975,#12976,#7452,.T.);
#16572=EDGE_CURVE('',#12976,#12976,#10635,.T.);
#16573=EDGE_CURVE('',#12975,#12974,#10636,.T.);
#16574=EDGE_CURVE('',#12974,#12977,#7453,.T.);
#16575=EDGE_CURVE('',#12977,#12977,#10637,.T.);
#16576=EDGE_CURVE('',#12978,#12979,#7454,.T.);
#16577=EDGE_CURVE('',#12980,#12978,#7455,.T.);
#16578=EDGE_CURVE('',#12981,#12980,#7456,.T.);
#16579=EDGE_CURVE('',#12982,#12981,#7457,.T.);
#16580=EDGE_CURVE('',#12983,#12982,#7458,.T.);
#16581=EDGE_CURVE('',#12979,#12983,#7459,.T.);
#16582=EDGE_CURVE('',#12984,#12979,#7460,.T.);
#16583=EDGE_CURVE('',#12985,#12984,#7461,.T.);
#16584=EDGE_CURVE('',#12985,#12978,#7462,.T.);
#16585=EDGE_CURVE('',#12986,#12985,#7463,.T.);
#16586=EDGE_CURVE('',#12986,#12980,#7464,.T.);
#16587=EDGE_CURVE('',#12987,#12986,#7465,.T.);
#16588=EDGE_CURVE('',#12987,#12981,#7466,.T.);
#16589=EDGE_CURVE('',#12988,#12987,#7467,.T.);
#16590=EDGE_CURVE('',#12988,#12982,#7468,.T.);
#16591=EDGE_CURVE('',#12989,#12988,#7469,.T.);
#16592=EDGE_CURVE('',#12989,#12983,#7470,.T.);
#16593=EDGE_CURVE('',#12984,#12989,#7471,.T.);
#23744=ORIENTED_EDGE('',*,*,#16565,.F.);
#23745=ORIENTED_EDGE('',*,*,#16566,.T.);
#23746=ORIENTED_EDGE('',*,*,#16567,.T.);
#23747=ORIENTED_EDGE('',*,*,#16566,.F.);
#23748=ORIENTED_EDGE('',*,*,#16567,.F.);
#23749=ORIENTED_EDGE('',*,*,#16568,.T.);
#23750=ORIENTED_EDGE('',*,*,#16569,.T.);
#23751=ORIENTED_EDGE('',*,*,#16568,.F.);
#23752=ORIENTED_EDGE('',*,*,#16570,.T.);
#23753=ORIENTED_EDGE('',*,*,#16571,.T.);
#23754=ORIENTED_EDGE('',*,*,#16572,.F.);
#23755=ORIENTED_EDGE('',*,*,#16571,.F.);
#23756=ORIENTED_EDGE('',*,*,#16573,.T.);
#23757=ORIENTED_EDGE('',*,*,#16570,.F.);
#23758=ORIENTED_EDGE('',*,*,#16574,.T.);
#23759=ORIENTED_EDGE('',*,*,#16575,.T.);
#23760=ORIENTED_EDGE('',*,*,#16574,.F.);
#23761=ORIENTED_EDGE('',*,*,#16573,.F.);
#23762=ORIENTED_EDGE('',*,*,#16572,.T.);
#23763=ORIENTED_EDGE('',*,*,#16569,.F.);
#23764=ORIENTED_EDGE('',*,*,#16576,.F.);
#23765=ORIENTED_EDGE('',*,*,#16577,.F.);
#23766=ORIENTED_EDGE('',*,*,#16578,.F.);
#23767=ORIENTED_EDGE('',*,*,#16579,.F.);
#23768=ORIENTED_EDGE('',*,*,#16580,.F.);
#23769=ORIENTED_EDGE('',*,*,#16581,.F.);
#23770=ORIENTED_EDGE('',*,*,#16565,.T.);
#23771=ORIENTED_EDGE('',*,*,#16575,.F.);
#23772=ORIENTED_EDGE('',*,*,#16576,.T.);
#23773=ORIENTED_EDGE('',*,*,#16582,.F.);
#23774=ORIENTED_EDGE('',*,*,#16583,.F.);
#23775=ORIENTED_EDGE('',*,*,#16584,.T.);
#23776=ORIENTED_EDGE('',*,*,#16577,.T.);
#23777=ORIENTED_EDGE('',*,*,#16584,.F.);
#23778=ORIENTED_EDGE('',*,*,#16585,.F.);
#23779=ORIENTED_EDGE('',*,*,#16586,.T.);
#23780=ORIENTED_EDGE('',*,*,#16578,.T.);
#23781=ORIENTED_EDGE('',*,*,#16586,.F.);
#23782=ORIENTED_EDGE('',*,*,#16587,.F.);
#23783=ORIENTED_EDGE('',*,*,#16588,.T.);
#23784=ORIENTED_EDGE('',*,*,#16579,.T.);
#23785=ORIENTED_EDGE('',*,*,#16588,.F.);
#23786=ORIENTED_EDGE('',*,*,#16589,.F.);
#23787=ORIENTED_EDGE('',*,*,#16590,.T.);
#23788=ORIENTED_EDGE('',*,*,#16580,.T.);
#23789=ORIENTED_EDGE('',*,*,#16590,.F.);
#23790=ORIENTED_EDGE('',*,*,#16591,.F.);
#23791=ORIENTED_EDGE('',*,*,#16592,.T.);
#23792=ORIENTED_EDGE('',*,*,#16581,.T.);
#23793=ORIENTED_EDGE('',*,*,#16592,.F.);
#23794=ORIENTED_EDGE('',*,*,#16593,.F.);
#23795=ORIENTED_EDGE('',*,*,#16582,.T.);
#23796=ORIENTED_EDGE('',*,*,#16583,.T.);
#23797=ORIENTED_EDGE('',*,*,#16593,.T.);
#23798=ORIENTED_EDGE('',*,*,#16591,.T.);
#23799=ORIENTED_EDGE('',*,*,#16589,.T.);
#23800=ORIENTED_EDGE('',*,*,#16587,.T.);
#23801=ORIENTED_EDGE('',*,*,#16585,.T.);
#24220=CYLINDRICAL_SURFACE('',#28681,5.);
#24221=CYLINDRICAL_SURFACE('',#28690,3.);
#25650=ADVANCED_FACE('',(#3697),#24220,.T.);
#25651=ADVANCED_FACE('',(#3698),#580,.T.);
#25652=ADVANCED_FACE('',(#3699),#581,.T.);
#25653=ADVANCED_FACE('',(#3700),#24221,.T.);
#25654=ADVANCED_FACE('',(#3701),#2259,.T.);
#25655=ADVANCED_FACE('',(#3702,#1496),#2260,.T.);
#25656=ADVANCED_FACE('',(#3703,#1497),#2261,.T.);
#25657=ADVANCED_FACE('',(#3704),#2262,.F.);
#25658=ADVANCED_FACE('',(#3705),#2263,.F.);
#25659=ADVANCED_FACE('',(#3706),#2264,.F.);
#25660=ADVANCED_FACE('',(#3707),#2265,.F.);
#25661=ADVANCED_FACE('',(#3708),#2266,.F.);
#25662=ADVANCED_FACE('',(#3709),#2267,.F.);
#25663=ADVANCED_FACE('',(#3710),#2268,.T.);
#25698=CLOSED_SHELL('',(#25650,#25651,#25652,#25653,#25654,#25655,#25656,
#25657,#25658,#25659,#25660,#25661,#25662,#25663));
#28680=AXIS2_PLACEMENT_3D('',#66523,#36001,#36002);
#28681=AXIS2_PLACEMENT_3D('',#66524,#36003,#36004);
#28682=AXIS2_PLACEMENT_3D('',#66526,#36005,#36006);
#28683=AXIS2_PLACEMENT_3D('',#66529,#36008,#36009);
#28684=AXIS2_PLACEMENT_3D('',#66530,#36010,#36011);
#28685=AXIS2_PLACEMENT_3D('',#66533,#36013,#36014);
#28686=AXIS2_PLACEMENT_3D('',#66534,#36015,#36016);
#28687=AXIS2_PLACEMENT_3D('',#66537,#36017,#36018);
#28688=AXIS2_PLACEMENT_3D('',#66540,#36020,#36021);
#28689=AXIS2_PLACEMENT_3D('',#66541,#36022,#36023);
#28690=AXIS2_PLACEMENT_3D('',#66542,#36024,#36025);
#28691=AXIS2_PLACEMENT_3D('',#66545,#36027,#36028);
#28692=AXIS2_PLACEMENT_3D('',#66546,#36029,#36030);
#28693=AXIS2_PLACEMENT_3D('',#66547,#36031,#36032);
#28694=AXIS2_PLACEMENT_3D('',#66560,#36039,#36040);
#28695=AXIS2_PLACEMENT_3D('',#66561,#36041,#36042);
#28696=AXIS2_PLACEMENT_3D('',#66567,#36046,#36047);
#28697=AXIS2_PLACEMENT_3D('',#66571,#36050,#36051);
#28698=AXIS2_PLACEMENT_3D('',#66575,#36054,#36055);
#28699=AXIS2_PLACEMENT_3D('',#66579,#36058,#36059);
#28700=AXIS2_PLACEMENT_3D('',#66583,#36062,#36063);
#28701=AXIS2_PLACEMENT_3D('',#66585,#36065,#36066);
#36001=DIRECTION('axis',(0.,0.,1.));
#36002=DIRECTION('refdir',(1.,0.,0.));
#36003=DIRECTION('center_axis',(1.,1.22464679914735E-16,0.));
#36004=DIRECTION('ref_axis',(-1.22464679914735E-16,1.,0.));
#36005=DIRECTION('center_axis',(1.,1.22464679914735E-16,0.));
#36006=DIRECTION('ref_axis',(-1.22464679914735E-16,1.,0.));
#36007=DIRECTION('',(-1.,-1.22464679914735E-16,0.));
#36008=DIRECTION('center_axis',(1.,1.22464679914735E-16,0.));
#36009=DIRECTION('ref_axis',(-1.22464679914735E-16,1.,0.));
#36010=DIRECTION('center_axis',(1.,1.22464679914735E-16,0.));
#36011=DIRECTION('ref_axis',(-1.22464679914735E-16,1.,0.));
#36012=DIRECTION('',(-0.707106781186546,0.707106781186549,8.65956056235495E-17));
#36013=DIRECTION('center_axis',(1.,1.22464679914735E-16,0.));
#36014=DIRECTION('ref_axis',(-1.22464679914735E-16,1.,0.));
#36015=DIRECTION('center_axis',(-1.,-1.22464679914735E-16,0.));
#36016=DIRECTION('ref_axis',(1.22464679914735E-16,-1.,0.));
#36017=DIRECTION('center_axis',(1.,1.22464679914735E-16,0.));
#36018=DIRECTION('ref_axis',(-1.22464679914735E-16,1.,0.));
#36019=DIRECTION('',(0.707106781186552,-0.707106781186543,8.65956056235488E-17));
#36020=DIRECTION('center_axis',(1.,1.22464679914735E-16,0.));
#36021=DIRECTION('ref_axis',(-1.22464679914735E-16,1.,0.));
#36022=DIRECTION('center_axis',(1.,1.22464679914735E-16,0.));
#36023=DIRECTION('ref_axis',(-1.22464679914735E-16,1.,0.));
#36024=DIRECTION('center_axis',(1.,1.22464679914735E-16,0.));
#36025=DIRECTION('ref_axis',(-1.22464679914735E-16,1.,0.));
#36026=DIRECTION('',(-1.,-1.22464679914735E-16,0.));
#36027=DIRECTION('center_axis',(1.,1.22464679914735E-16,0.));
#36028=DIRECTION('ref_axis',(-1.22464679914735E-16,1.,0.));
#36029=DIRECTION('center_axis',(1.,1.22464679914735E-16,0.));
#36030=DIRECTION('ref_axis',(-1.22464679914735E-16,1.,0.));
#36031=DIRECTION('center_axis',(-1.,-1.22464679914735E-16,0.));
#36032=DIRECTION('ref_axis',(1.22464679914735E-16,-1.,0.));
#36033=DIRECTION('',(0.,0.5,-0.866025403784439));
#36034=DIRECTION('',(0.,1.,0.));
#36035=DIRECTION('',(0.,0.5,0.866025403784439));
#36036=DIRECTION('',(0.,-0.5,0.866025403784438));
#36037=DIRECTION('',(0.,-1.,-1.50231459873716E-16));
#36038=DIRECTION('',(0.,-0.5,-0.866025403784439));
#36039=DIRECTION('center_axis',(1.,1.22464679914735E-16,0.));
#36040=DIRECTION('ref_axis',(-1.22464679914735E-16,1.,0.));
#36041=DIRECTION('center_axis',(-1.06057523872491E-16,0.866025403784439,
0.5));
#36042=DIRECTION('ref_axis',(-5.09861652542584E-33,-0.5,0.866025403784439));
#36043=DIRECTION('',(-1.,-1.22464679914735E-16,0.));
#36044=DIRECTION('',(0.,0.5,-0.866025403784439));
#36045=DIRECTION('',(-1.,-1.22464679914735E-16,0.));
#36046=DIRECTION('center_axis',(0.,0.,1.));
#36047=DIRECTION('ref_axis',(1.,0.,0.));
#36048=DIRECTION('',(0.,1.,0.));
#36049=DIRECTION('',(-1.,-1.22464679914735E-16,0.));
#36050=DIRECTION('center_axis',(1.06057523872491E-16,-0.866025403784439,
0.5));
#36051=DIRECTION('ref_axis',(-8.4117933897259E-34,-0.5,-0.866025403784439));
#36052=DIRECTION('',(0.,0.5,0.866025403784439));
#36053=DIRECTION('',(-1.,-1.22464679914735E-16,0.));
#36054=DIRECTION('center_axis',(1.06057523872491E-16,-0.866025403784439,
-0.5));
#36055=DIRECTION('ref_axis',(-5.93979586439842E-33,0.5,-0.866025403784439));
#36056=DIRECTION('',(0.,-0.5,0.866025403784438));
#36057=DIRECTION('',(-1.,-1.22464679914735E-16,0.));
#36058=DIRECTION('center_axis',(-1.8398047646558E-32,1.50231459873716E-16,
-1.));
#36059=DIRECTION('ref_axis',(0.,1.,1.50231459873716E-16));
#36060=DIRECTION('',(0.,-1.,-1.50231459873716E-16));
#36061=DIRECTION('',(-1.,-1.22464679914735E-16,0.));
#36062=DIRECTION('center_axis',(-1.06057523872491E-16,0.866025403784439,
-0.5));
#36063=DIRECTION('ref_axis',(2.96989793219921E-33,0.5,0.866025403784439));
#36064=DIRECTION('',(0.,-0.5,-0.866025403784439));
#36065=DIRECTION('center_axis',(-1.,0.,0.));
#36066=DIRECTION('ref_axis',(0.,0.,1.));
#66523=CARTESIAN_POINT('',(0.,0.,0.));
#66524=CARTESIAN_POINT('Origin',(25.,2.32682891837997E-15,0.));
#66525=CARTESIAN_POINT('',(0.,-5.,-6.12323399573677E-16));
#66526=CARTESIAN_POINT('Origin',(0.,-7.34788079488413E-16,0.));
#66527=CARTESIAN_POINT('',(-5.4,-5.,-6.12323399573677E-16));
#66528=CARTESIAN_POINT('',(25.,-5.,-6.12323399573677E-16));
#66529=CARTESIAN_POINT('Origin',(-5.4,-1.39609735102798E-15,0.));
#66530=CARTESIAN_POINT('Origin',(-5.4,-1.39609735102798E-15,0.));
#66531=CARTESIAN_POINT('',(-6.,-4.4,-5.38844591624836E-16));
#66532=CARTESIAN_POINT('',(-5.4,-5.,-6.12323399573677E-16));
#66533=CARTESIAN_POINT('Origin',(-6.,-1.46957615897682E-15,0.));
#66534=CARTESIAN_POINT('Origin',(25.,2.32682891837997E-15,0.));
#66535=CARTESIAN_POINT('',(24.4585,-3.,3.67394039744206E-16));
#66536=CARTESIAN_POINT('',(24.4585,3.,-3.67394039744206E-16));
#66537=CARTESIAN_POINT('Origin',(24.4585,2.26051429420614E-15,0.));
#66538=CARTESIAN_POINT('',(25.,2.4585,-3.01079415570377E-16));
#66539=CARTESIAN_POINT('',(25.,2.4585,-3.01079415570377E-16));
#66540=CARTESIAN_POINT('Origin',(25.,2.32682891837997E-15,0.));
#66541=CARTESIAN_POINT('Origin',(24.4585,2.26051429420614E-15,0.));
#66542=CARTESIAN_POINT('Origin',(25.,2.32682891837997E-15,0.));
#66543=CARTESIAN_POINT('',(0.,-3.,-3.67394039744206E-16));
#66544=CARTESIAN_POINT('',(25.,-3.,-3.67394039744206E-16));
#66545=CARTESIAN_POINT('Origin',(0.,-7.34788079488413E-16,0.));
#66546=CARTESIAN_POINT('Origin',(25.,2.4585,0.));
#66547=CARTESIAN_POINT('Origin',(-6.,-1.46957615897682E-15,0.));
#66548=CARTESIAN_POINT('',(-6.,1.44337567297406,2.5));
#66549=CARTESIAN_POINT('',(-6.,2.88675134594813,0.));
#66550=CARTESIAN_POINT('',(-6.,1.44337567297406,2.5));
#66551=CARTESIAN_POINT('',(-6.,-1.44337567297407,2.5));
#66552=CARTESIAN_POINT('',(-6.,-1.44337567297407,2.5));
#66553=CARTESIAN_POINT('',(-6.,-2.88675134594813,-7.77133304087269E-16));
#66554=CARTESIAN_POINT('',(-6.,-2.88675134594813,-7.77133304087269E-16));
#66555=CARTESIAN_POINT('',(-6.,-1.44337567297407,-2.5));
#66556=CARTESIAN_POINT('',(-6.,-1.44337567297407,-2.5));
#66557=CARTESIAN_POINT('',(-6.,1.44337567297406,-2.5));
#66558=CARTESIAN_POINT('',(-6.,1.44337567297406,-2.5));
#66559=CARTESIAN_POINT('',(-6.,2.88675134594813,3.50584097974525E-17));
#66560=CARTESIAN_POINT('Origin',(1.22464679914735E-16,3.,0.));
#66561=CARTESIAN_POINT('Origin',(-3.,1.44337567297406,2.5));
#66562=CARTESIAN_POINT('',(-3.,2.88675134594813,3.50584097974525E-17));
#66563=CARTESIAN_POINT('',(-3.,2.88675134594813,3.50584097974525E-17));
#66564=CARTESIAN_POINT('',(-3.,1.44337567297406,2.5));
#66565=CARTESIAN_POINT('',(-3.,1.44337567297406,2.5));
#66566=CARTESIAN_POINT('',(-3.,1.44337567297406,2.5));
#66567=CARTESIAN_POINT('Origin',(-3.,-1.44337567297407,2.5));
#66568=CARTESIAN_POINT('',(-3.,-1.44337567297407,2.5));
#66569=CARTESIAN_POINT('',(-3.,-1.44337567297407,2.5));
#66570=CARTESIAN_POINT('',(-3.,-1.44337567297407,2.5));
#66571=CARTESIAN_POINT('Origin',(-3.,-2.88675134594813,-7.77133304087269E-16));
#66572=CARTESIAN_POINT('',(-3.,-2.88675134594813,-7.77133304087269E-16));
#66573=CARTESIAN_POINT('',(-3.,-2.88675134594813,-7.77133304087269E-16));
#66574=CARTESIAN_POINT('',(-3.,-2.88675134594813,-7.77133304087269E-16));
#66575=CARTESIAN_POINT('Origin',(-3.,-1.44337567297406,-2.5));
#66576=CARTESIAN_POINT('',(-3.,-1.44337567297406,-2.5));
#66577=CARTESIAN_POINT('',(-3.,-1.44337567297406,-2.5));
#66578=CARTESIAN_POINT('',(-3.,-1.44337567297406,-2.5));
#66579=CARTESIAN_POINT('Origin',(-3.,1.44337567297407,-2.5));
#66580=CARTESIAN_POINT('',(-3.,1.44337567297407,-2.5));
#66581=CARTESIAN_POINT('',(-3.,1.44337567297407,-2.5));
#66582=CARTESIAN_POINT('',(-3.,1.44337567297407,-2.5));
#66583=CARTESIAN_POINT('Origin',(-3.,2.88675134594813,3.50584097974525E-17));
#66584=CARTESIAN_POINT('',(-3.,2.88675134594813,3.50584097974525E-17));
#66585=CARTESIAN_POINT('Origin',(-3.,3.67394039744206E-16,0.));
#66679=UNCERTAINTY_MEASURE_WITH_UNIT(LENGTH_MEASURE(0.01),#66722,
'DISTANCE_ACCURACY_VALUE',
'Maximum model space distance between geometric entities at asserted c
onnectivities');
#66680=UNCERTAINTY_MEASURE_WITH_UNIT(LENGTH_MEASURE(0.01),#66722,
'DISTANCE_ACCURACY_VALUE',
'Maximum model space distance between geometric entities at asserted c
onnectivities');
#66720=(
GEOMETRIC_REPRESENTATION_CONTEXT(3)
GLOBAL_UNCERTAINTY_ASSIGNED_CONTEXT((#66679))
GLOBAL_UNIT_ASSIGNED_CONTEXT((#66722,#66724,#66725))
REPRESENTATION_CONTEXT('','3D')
);
#66721=(
GEOMETRIC_REPRESENTATION_CONTEXT(3)
GLOBAL_UNCERTAINTY_ASSIGNED_CONTEXT((#66680))
GLOBAL_UNIT_ASSIGNED_CONTEXT((#66722,#66724,#66725))
REPRESENTATION_CONTEXT('','3D')
);
#66722=(
LENGTH_UNIT()
NAMED_UNIT(*)
SI_UNIT(.MILLI.,.METRE.)
);
#66724=(
NAMED_UNIT(*)
PLANE_ANGLE_UNIT()
SI_UNIT($,.RADIAN.)
);
#66725=(
NAMED_UNIT(*)
SI_UNIT($,.STERADIAN.)
SOLID_ANGLE_UNIT()
);
#66765=SHAPE_DEFINITION_REPRESENTATION(#66835,#66929);
#66835=PRODUCT_DEFINITION_SHAPE('',$,#66970);
#66929=SHAPE_REPRESENTATION('',(#28680),#66720);
#66930=PRODUCT_DEFINITION_CONTEXT('part definition',#67052,'design');
#66970=PRODUCT_DEFINITION('Socket head cap screw M6x25',
'Socket Head Cap Screw M6x25',#67010,#66930);
#67010=PRODUCT_DEFINITION_FORMATION('',$,#67093);
#67052=APPLICATION_CONTEXT(
'Core Data for Automotive Mechanical Design Process');
#67053=PRODUCT_CONTEXT('part definition',#67052,'mechanical');
#67093=PRODUCT('Socket head cap screw M6x25',
'Socket Head Cap Screw M6x25',$,(#67053));
#67095=PRESENTATION_STYLE_ASSIGNMENT((#67097));
#67097=SURFACE_STYLE_USAGE(.BOTH.,#67099);
#67099=SURFACE_SIDE_STYLE('',(#67101));
#67101=SURFACE_STYLE_FILL_AREA(#67103);
#67103=FILL_AREA_STYLE('Opaque(202,209,238)',(#67105));
#67105=FILL_AREA_STYLE_COLOUR('Opaque(202,209,238)',#67107);
#67107=COLOUR_RGB('Opaque(202,209,238)',0.792156862745098,0.819607843137255,
0.933333333333333);
ENDSEC;
END-ISO-10303-21;
